ISO-10303-21;
HEADER;
/* Generated by software containing ST-Developer
 * from STEP Tools, Inc. (www.steptools.com) 
 */

FILE_DESCRIPTION(
/* description */ ('PAT-083'),
/* implementation_level */ '2;1');

FILE_NAME(
/* name */ 'Poppet and stem.step',
/* time_stamp */ '2026-10-29T20:18:00-07:00',
/* author */ (''),
/* organization */ (''),
/* preprocessor_version */ 'ST-DEVELOPER v20.2',
/* originating_system */ 'Autodesk Translation Framework v15.17.0.0',
/* authorisation */ '');

FILE_SCHEMA (('AUTOMOTIVE_DESIGN { 1 0 10303 214 3 1 1 }'));
ENDSEC;

DATA;
#10=MECHANICAL_DESIGN_GEOMETRIC_PRESENTATION_REPRESENTATION('',(#235),#8428);
#187=SHAPE_REPRESENTATION_RELATIONSHIP('SRR','None',#8521,#211);
#211=ADVANCED_BREP_SHAPE_REPRESENTATION('',(#259),#8410);
#235=STYLED_ITEM('',(#8719),#259);
#259=MANIFOLD_SOLID_BREP('Body1',#3681);
#300=FACE_BOUND('',#819,.T.);
#301=FACE_BOUND('',#822,.T.);
#302=FACE_BOUND('',#824,.T.);
#303=FACE_BOUND('',#831,.T.);
#395=PLANE('',#4087);
#396=PLANE('',#4092);
#397=PLANE('',#4095);
#398=PLANE('',#4102);
#399=PLANE('',#4106);
#400=PLANE('',#4107);
#560=FACE_OUTER_BOUND('',#818,.T.);
#561=FACE_OUTER_BOUND('',#820,.T.);
#562=FACE_OUTER_BOUND('',#821,.T.);
#563=FACE_OUTER_BOUND('',#823,.T.);
#564=FACE_OUTER_BOUND('',#825,.T.);
#565=FACE_OUTER_BOUND('',#826,.T.);
#566=FACE_OUTER_BOUND('',#827,.T.);
#567=FACE_OUTER_BOUND('',#828,.T.);
#568=FACE_OUTER_BOUND('',#829,.T.);
#569=FACE_OUTER_BOUND('',#830,.T.);
#570=FACE_OUTER_BOUND('',#832,.T.);
#818=EDGE_LOOP('',(#2708));
#819=EDGE_LOOP('',(#2709));
#820=EDGE_LOOP('',(#2710,#2711,#2712,#2713));
#821=EDGE_LOOP('',(#2714));
#822=EDGE_LOOP('',(#2715));
#823=EDGE_LOOP('',(#2716));
#824=EDGE_LOOP('',(#2717));
#825=EDGE_LOOP('',(#2718,#2719,#2720,#2721));
#826=EDGE_LOOP('',(#2722,#2723,#2724,#2725));
#827=EDGE_LOOP('',(#2726,#2727,#2728,#2729));
#828=EDGE_LOOP('',(#2730));
#829=EDGE_LOOP('',(#2731,#2732,#2733,#2734));
#830=EDGE_LOOP('',(#2735));
#831=EDGE_LOOP('',(#2736));
#832=EDGE_LOOP('',(#2737));
#1110=LINE('',#6043,#1354);
#1111=LINE('',#6055,#1355);
#1112=LINE('',#6058,#1356);
#1113=LINE('',#6061,#1357);
#1114=LINE('',#6067,#1358);
#1354=VECTOR('',#4756,0.4);
#1355=VECTOR('',#4771,0.4);
#1356=VECTOR('',#4774,0.15);
#1357=VECTOR('',#4779,0.15);
#1358=VECTOR('',#4786,0.4);
#1578=CIRCLE('',#4088,0.4);
#1579=CIRCLE('',#4089,0.15);
#1580=CIRCLE('',#4091,0.4);
#1581=CIRCLE('',#4093,0.4);
#1582=CIRCLE('',#4094,0.15);
#1583=CIRCLE('',#4096,0.4);
#1584=CIRCLE('',#4097,0.15);
#1585=CIRCLE('',#4100,0.15);
#1586=CIRCLE('',#4104,0.4);
#1587=CIRCLE('',#4105,0.4);
#1791=VERTEX_POINT('',#6036);
#1792=VERTEX_POINT('',#6038);
#1793=VERTEX_POINT('',#6041);
#1794=VERTEX_POINT('',#6045);
#1795=VERTEX_POINT('',#6047);
#1796=VERTEX_POINT('',#6050);
#1797=VERTEX_POINT('',#6052);
#1798=VERTEX_POINT('',#6057);
#1799=VERTEX_POINT('',#6064);
#1800=VERTEX_POINT('',#6066);
#2130=EDGE_CURVE('',#1791,#1791,#1578,.T.);
#2131=EDGE_CURVE('',#1792,#1792,#1579,.T.);
#2132=EDGE_CURVE('',#1793,#1793,#1580,.T.);
#2133=EDGE_CURVE('',#1793,#1791,#1110,.T.);
#2134=EDGE_CURVE('',#1794,#1794,#1581,.T.);
#2135=EDGE_CURVE('',#1795,#1795,#1582,.T.);
#2136=EDGE_CURVE('',#1796,#1796,#1583,.T.);
#2137=EDGE_CURVE('',#1797,#1797,#1584,.T.);
#2138=EDGE_CURVE('',#1794,#1796,#1111,.T.);
#2139=EDGE_CURVE('',#1797,#1798,#1112,.T.);
#2140=EDGE_CURVE('',#1798,#1798,#1585,.T.);
#2141=EDGE_CURVE('',#1792,#1795,#1113,.T.);
#2142=EDGE_CURVE('',#1799,#1799,#1586,.T.);
#2143=EDGE_CURVE('',#1799,#1800,#1114,.T.);
#2144=EDGE_CURVE('',#1800,#1800,#1587,.T.);
#2708=ORIENTED_EDGE('',*,*,#2130,.F.);
#2709=ORIENTED_EDGE('',*,*,#2131,.F.);
#2710=ORIENTED_EDGE('',*,*,#2132,.F.);
#2711=ORIENTED_EDGE('',*,*,#2133,.T.);
#2712=ORIENTED_EDGE('',*,*,#2130,.T.);
#2713=ORIENTED_EDGE('',*,*,#2133,.F.);
#2714=ORIENTED_EDGE('',*,*,#2134,.T.);
#2715=ORIENTED_EDGE('',*,*,#2135,.F.);
#2716=ORIENTED_EDGE('',*,*,#2136,.F.);
#2717=ORIENTED_EDGE('',*,*,#2137,.F.);
#2718=ORIENTED_EDGE('',*,*,#2134,.F.);
#2719=ORIENTED_EDGE('',*,*,#2138,.T.);
#2720=ORIENTED_EDGE('',*,*,#2136,.T.);
#2721=ORIENTED_EDGE('',*,*,#2138,.F.);
#2722=ORIENTED_EDGE('',*,*,#2137,.T.);
#2723=ORIENTED_EDGE('',*,*,#2139,.T.);
#2724=ORIENTED_EDGE('',*,*,#2140,.F.);
#2725=ORIENTED_EDGE('',*,*,#2139,.F.);
#2726=ORIENTED_EDGE('',*,*,#2131,.T.);
#2727=ORIENTED_EDGE('',*,*,#2141,.T.);
#2728=ORIENTED_EDGE('',*,*,#2135,.T.);
#2729=ORIENTED_EDGE('',*,*,#2141,.F.);
#2730=ORIENTED_EDGE('',*,*,#2132,.T.);
#2731=ORIENTED_EDGE('',*,*,#2142,.F.);
#2732=ORIENTED_EDGE('',*,*,#2143,.T.);
#2733=ORIENTED_EDGE('',*,*,#2144,.T.);
#2734=ORIENTED_EDGE('',*,*,#2143,.F.);
#2735=ORIENTED_EDGE('',*,*,#2142,.T.);
#2736=ORIENTED_EDGE('',*,*,#2140,.T.);
#2737=ORIENTED_EDGE('',*,*,#2144,.F.);
#3390=CYLINDRICAL_SURFACE('',#4090,0.4);
#3391=CYLINDRICAL_SURFACE('',#4098,0.4);
#3392=CYLINDRICAL_SURFACE('',#4099,0.15);
#3393=CYLINDRICAL_SURFACE('',#4101,0.15);
#3394=CYLINDRICAL_SURFACE('',#4103,0.4);
#3507=ADVANCED_FACE('',(#560,#300),#395,.F.);
#3508=ADVANCED_FACE('',(#561),#3390,.T.);
#3509=ADVANCED_FACE('',(#562,#301),#396,.T.);
#3510=ADVANCED_FACE('',(#563,#302),#397,.F.);
#3511=ADVANCED_FACE('',(#564),#3391,.T.);
#3512=ADVANCED_FACE('',(#565),#3392,.T.);
#3513=ADVANCED_FACE('',(#566),#3393,.T.);
#3514=ADVANCED_FACE('',(#567),#398,.T.);
#3515=ADVANCED_FACE('',(#568),#3394,.T.);
#3516=ADVANCED_FACE('',(#569,#303),#399,.T.);
#3517=ADVANCED_FACE('',(#570),#400,.F.);
#3681=CLOSED_SHELL('',(#3507,#3508,#3509,#3510,#3511,#3512,#3513,#3514,
#3515,#3516,#3517));
#4086=AXIS2_PLACEMENT_3D('',#6034,#4744,#4745);
#4087=AXIS2_PLACEMENT_3D('',#6035,#4746,#4747);
#4088=AXIS2_PLACEMENT_3D('',#6037,#4748,#4749);
#4089=AXIS2_PLACEMENT_3D('',#6039,#4750,#4751);
#4090=AXIS2_PLACEMENT_3D('',#6040,#4752,#4753);
#4091=AXIS2_PLACEMENT_3D('',#6042,#4754,#4755);
#4092=AXIS2_PLACEMENT_3D('',#6044,#4757,#4758);
#4093=AXIS2_PLACEMENT_3D('',#6046,#4759,#4760);
#4094=AXIS2_PLACEMENT_3D('',#6048,#4761,#4762);
#4095=AXIS2_PLACEMENT_3D('',#6049,#4763,#4764);
#4096=AXIS2_PLACEMENT_3D('',#6051,#4765,#4766);
#4097=AXIS2_PLACEMENT_3D('',#6053,#4767,#4768);
#4098=AXIS2_PLACEMENT_3D('',#6054,#4769,#4770);
#4099=AXIS2_PLACEMENT_3D('',#6056,#4772,#4773);
#4100=AXIS2_PLACEMENT_3D('',#6059,#4775,#4776);
#4101=AXIS2_PLACEMENT_3D('',#6060,#4777,#4778);
#4102=AXIS2_PLACEMENT_3D('',#6062,#4780,#4781);
#4103=AXIS2_PLACEMENT_3D('',#6063,#4782,#4783);
#4104=AXIS2_PLACEMENT_3D('',#6065,#4784,#4785);
#4105=AXIS2_PLACEMENT_3D('',#6068,#4787,#4788);
#4106=AXIS2_PLACEMENT_3D('',#6069,#4789,#4790);
#4107=AXIS2_PLACEMENT_3D('',#6070,#4791,#4792);
#4744=DIRECTION('axis',(0.,0.,1.));
#4745=DIRECTION('refdir',(1.,0.,0.));
#4746=DIRECTION('center_axis',(0.,0.,1.));
#4747=DIRECTION('ref_axis',(1.,0.,0.));
#4748=DIRECTION('center_axis',(0.,0.,1.));
#4749=DIRECTION('ref_axis',(1.,0.,0.));
#4750=DIRECTION('center_axis',(0.,0.,-1.));
#4751=DIRECTION('ref_axis',(1.,0.,0.));
#4752=DIRECTION('center_axis',(0.,0.,1.));
#4753=DIRECTION('ref_axis',(1.,0.,0.));
#4754=DIRECTION('center_axis',(0.,0.,1.));
#4755=DIRECTION('ref_axis',(1.,0.,0.));
#4756=DIRECTION('',(0.,0.,-1.));
#4757=DIRECTION('center_axis',(0.,0.,1.));
#4758=DIRECTION('ref_axis',(1.,0.,0.));
#4759=DIRECTION('center_axis',(0.,0.,1.));
#4760=DIRECTION('ref_axis',(1.,0.,0.));
#4761=DIRECTION('center_axis',(0.,0.,1.));
#4762=DIRECTION('ref_axis',(1.,0.,0.));
#4763=DIRECTION('center_axis',(0.,0.,1.));
#4764=DIRECTION('ref_axis',(1.,0.,0.));
#4765=DIRECTION('center_axis',(0.,0.,1.));
#4766=DIRECTION('ref_axis',(1.,0.,0.));
#4767=DIRECTION('center_axis',(0.,0.,-1.));
#4768=DIRECTION('ref_axis',(1.,0.,0.));
#4769=DIRECTION('center_axis',(0.,0.,1.));
#4770=DIRECTION('ref_axis',(1.,0.,0.));
#4771=DIRECTION('',(0.,0.,-1.));
#4772=DIRECTION('center_axis',(0.,0.,1.));
#4773=DIRECTION('ref_axis',(1.,0.,0.));
#4774=DIRECTION('',(0.,0.,-1.));
#4775=DIRECTION('center_axis',(0.,0.,-1.));
#4776=DIRECTION('ref_axis',(1.,0.,0.));
#4777=DIRECTION('center_axis',(0.,0.,1.));
#4778=DIRECTION('ref_axis',(1.,0.,0.));
#4779=DIRECTION('',(0.,0.,-1.));
#4780=DIRECTION('center_axis',(0.,0.,1.));
#4781=DIRECTION('ref_axis',(1.,0.,0.));
#4782=DIRECTION('center_axis',(0.,0.,1.));
#4783=DIRECTION('ref_axis',(1.,0.,0.));
#4784=DIRECTION('center_axis',(0.,0.,1.));
#4785=DIRECTION('ref_axis',(1.,0.,0.));
#4786=DIRECTION('',(0.,0.,-1.));
#4787=DIRECTION('center_axis',(0.,0.,1.));
#4788=DIRECTION('ref_axis',(1.,0.,0.));
#4789=DIRECTION('center_axis',(0.,0.,1.));
#4790=DIRECTION('ref_axis',(1.,0.,0.));
#4791=DIRECTION('center_axis',(0.,0.,1.));
#4792=DIRECTION('ref_axis',(1.,0.,0.));
#6034=CARTESIAN_POINT('',(0.,0.,0.));
#6035=CARTESIAN_POINT('Origin',(0.,0.,5.3));
#6036=CARTESIAN_POINT('',(-0.4,-4.89858719658941E-17,5.3));
#6037=CARTESIAN_POINT('Origin',(0.,0.,5.3));
#6038=CARTESIAN_POINT('',(-0.15,1.83697019872103E-17,5.3));
#6039=CARTESIAN_POINT('Origin',(0.,0.,5.3));
#6040=CARTESIAN_POINT('Origin',(0.,0.,5.3));
#6041=CARTESIAN_POINT('',(-0.4,-4.89858719658941E-17,5.5));
#6042=CARTESIAN_POINT('Origin',(0.,0.,5.5));
#6043=CARTESIAN_POINT('',(-0.4,-4.89858719658941E-17,5.3));
#6044=CARTESIAN_POINT('Origin',(0.,0.,4.8));
#6045=CARTESIAN_POINT('',(-0.4,-4.89858719658941E-17,4.8));
#6046=CARTESIAN_POINT('Origin',(0.,0.,4.8));
#6047=CARTESIAN_POINT('',(-0.15,-1.83697019872103E-17,4.8));
#6048=CARTESIAN_POINT('Origin',(0.,0.,4.8));
#6049=CARTESIAN_POINT('Origin',(0.,0.,4.6));
#6050=CARTESIAN_POINT('',(-0.4,-4.89858719658941E-17,4.6));
#6051=CARTESIAN_POINT('Origin',(0.,0.,4.6));
#6052=CARTESIAN_POINT('',(-0.15,1.83697019872103E-17,4.6));
#6053=CARTESIAN_POINT('Origin',(0.,0.,4.6));
#6054=CARTESIAN_POINT('Origin',(0.,0.,4.6));
#6055=CARTESIAN_POINT('',(-0.4,-4.89858719658941E-17,4.6));
#6056=CARTESIAN_POINT('Origin',(0.,0.,2.4));
#6057=CARTESIAN_POINT('',(-0.15,-1.83697019872103E-17,2.4));
#6058=CARTESIAN_POINT('',(-0.15,-1.83697019872103E-17,2.4));
#6059=CARTESIAN_POINT('Origin',(0.,0.,2.4));
#6060=CARTESIAN_POINT('Origin',(0.,0.,2.4));
#6061=CARTESIAN_POINT('',(-0.15,-1.83697019872103E-17,2.4));
#6062=CARTESIAN_POINT('Origin',(0.,0.,5.5));
#6063=CARTESIAN_POINT('Origin',(0.,0.,2.2));
#6064=CARTESIAN_POINT('',(-0.4,-4.89858719658941E-17,2.4));
#6065=CARTESIAN_POINT('Origin',(0.,0.,2.4));
#6066=CARTESIAN_POINT('',(-0.4,-4.89858719658941E-17,2.2));
#6067=CARTESIAN_POINT('',(-0.4,-4.89858719658941E-17,2.2));
#6068=CARTESIAN_POINT('Origin',(0.,0.,2.2));
#6069=CARTESIAN_POINT('Origin',(0.,0.,2.4));
#6070=CARTESIAN_POINT('Origin',(0.,0.,2.2));
#8384=UNCERTAINTY_MEASURE_WITH_UNIT(LENGTH_MEASURE(0.001),#8429,
'DISTANCE_ACCURACY_VALUE',
'Maximum model space distance between geometric entities at asserted c
onnectivities');
#8402=UNCERTAINTY_MEASURE_WITH_UNIT(LENGTH_MEASURE(0.001),#8429,
'DISTANCE_ACCURACY_VALUE',
'Maximum model space distance between geometric entities at asserted c
onnectivities');
#8410=(
GEOMETRIC_REPRESENTATION_CONTEXT(3)
GLOBAL_UNCERTAINTY_ASSIGNED_CONTEXT((#8384))
GLOBAL_UNIT_ASSIGNED_CONTEXT((#8429,#8431,#8432))
REPRESENTATION_CONTEXT('','3D')
);
#8428=(
GEOMETRIC_REPRESENTATION_CONTEXT(3)
GLOBAL_UNCERTAINTY_ASSIGNED_CONTEXT((#8402))
GLOBAL_UNIT_ASSIGNED_CONTEXT((#8429,#8431,#8432))
REPRESENTATION_CONTEXT('','3D')
);
#8429=(
LENGTH_UNIT()
NAMED_UNIT(*)
SI_UNIT(.CENTI.,.METRE.)
);
#8431=(
NAMED_UNIT(*)
PLANE_ANGLE_UNIT()
SI_UNIT($,.RADIAN.)
);
#8432=(
NAMED_UNIT(*)
SI_UNIT($,.STERADIAN.)
SOLID_ANGLE_UNIT()
);
#8440=SHAPE_DEFINITION_REPRESENTATION(#8465,#8521);
#8465=PRODUCT_DEFINITION_SHAPE('',$,#8547);
#8521=SHAPE_REPRESENTATION('',(#4086),#8410);
#8539=PRODUCT_DEFINITION_CONTEXT('part definition',#8616,'design');
#8547=PRODUCT_DEFINITION('Poppet and stem','Poppet and stem',#8572,
#8539);
#8572=PRODUCT_DEFINITION_FORMATION('',$,#8625);
#8616=APPLICATION_CONTEXT(
'Core Data for Automotive Mechanical Design Process');
#8617=PRODUCT_CONTEXT('part definition',#8616,'mechanical');
#8625=PRODUCT('Poppet and stem','Poppet and stem',
'Poppet and stem',(#8617));
#8713=COLOUR_RGB('Off White',0.89,0.88,0.83);
#8714=FILL_AREA_STYLE_COLOUR('',#8713);
#8715=FILL_AREA_STYLE('',(#8714));
#8716=SURFACE_STYLE_FILL_AREA(#8715);
#8717=SURFACE_SIDE_STYLE('',(#8716));
#8718=SURFACE_STYLE_USAGE(.BOTH.,#8717);
#8719=PRESENTATION_STYLE_ASSIGNMENT((#8718));
ENDSEC;
END-ISO-10303-21;
